ISO-10303-21;
HEADER;
FILE_DESCRIPTION (('STEP AP214'),
    '1' );
FILE_NAME ('flat washer narrow_am_B18.22M - Plain washer, 10 mm, narrow.step',
    '2026-10-24T15:53:57',
    ( '' ),
    ( '' ),
    'SwSTEP 2.0',
    'SolidWorks 2025',
    '' );
FILE_SCHEMA (( 'AUTOMOTIVE_DESIGN' ));
ENDSEC;

DATA;
#44=CARTESIAN_POINT ( 'NONE',  ( -2.300000000000024247, 0.000000000000000000, 0.000000000000000000 ) ) ;
#81=FACE_OUTER_BOUND ( 'NONE', #5518, .T. ) ;
#89=DIRECTION ( 'NONE',  ( -1.000000000000000000, 0.000000000000000000, 0.000000000000000000 ) ) ;
#107=CARTESIAN_POINT ( 'NONE',  ( -2.300000000000024247, 0.000000000000000000, 0.000000000000000000 ) ) ;
#130=DIRECTION ( 'NONE',  ( 0.000000000000000000, 0.000000000000000000, 1.000000000000000000 ) ) ;
#143=DIRECTION ( 'NONE',  ( 0.000000000000000000, 0.000000000000000000, 1.000000000000000000 ) ) ;
#155=DIRECTION ( 'NONE',  ( 0.000000000000000000, 0.000000000000000000, 1.000000000000000000 ) ) ;
#194=CARTESIAN_POINT ( 'NONE',  ( -34.92499999999998295, 0.000000000000000000, 0.000000000000000000 ) ) ;
#216=ORIENTED_EDGE ( 'NONE', *, *, #7702, .T. ) ;
#238=FACE_BOUND ( 'NONE', #6984, .T. ) ;
#275=ORIENTED_EDGE ( 'NONE', *, *, #2858, .F. ) ;
#296=EDGE_CURVE ( 'NONE', #662, #1055, #1974, .T. ) ;
#355=CIRCLE ( 'NONE', #3273, 5.559999999999998721 ) ;
#376=( NAMED_UNIT ( * ) PLANE_ANGLE_UNIT ( ) SI_UNIT ( $, .RADIAN. ) );
#580=AXIS2_PLACEMENT_3D ( 'NONE', #4509, #3851, #2423 ) ;
#586=DIRECTION ( 'NONE',  ( -1.000000000000000000, 0.000000000000000000, 0.000000000000000000 ) ) ;
#592=EDGE_CURVE ( 'NONE', #6230, #3933, #4357, .T. ) ;
#621=DIRECTION ( 'NONE',  ( -1.000000000000000000, 0.000000000000000000, 0.000000000000000000 ) ) ;
#662=VERTEX_POINT ( 'NONE', #5028 ) ;
#691=CIRCLE ( 'NONE', #4027, 10.00000000000000178 ) ;
#716=ADVANCED_FACE ( 'NONE', ( #5109, #6318 ), #7768, .F. ) ;
#762=CYLINDRICAL_SURFACE ( 'NONE', #8377, 10.00000000000000178 ) ;
#814=CARTESIAN_POINT ( 'NONE',  ( -2.300000000000024247, 10.00000000000000888, 0.000000000000000000 ) ) ;
#841=ADVANCED_BREP_SHAPE_REPRESENTATION ( '', ( #2776, #7563 ), #4924 ) ;
#845=STYLED_ITEM('',(#8670),#2776);
#859=DIRECTION ( 'NONE',  ( 0.000000000000000000, 0.000000000000000000, -1.000000000000000000 ) ) ;
#944=PRODUCT_DEFINITION ( 'UNKNOWN', '', #5930, #3848 ) ;
#1004=ORIENTED_EDGE ( 'NONE', *, *, #1173, .T. ) ;
#1055=VERTEX_POINT ( 'NONE', #4228 ) ;
#1071=VERTEX_POINT ( 'NONE', #8236 ) ;
#1118=CIRCLE ( 'NONE', #8079, 10.00000000000000178 ) ;
#1125=DIRECTION ( 'NONE',  ( -1.000000000000000000, 0.000000000000000000, 0.000000000000000000 ) ) ;
#1167=ORIENTED_EDGE ( 'NONE', *, *, #2419, .F. ) ;
#1173=EDGE_CURVE ( 'NONE', #3827, #1071, #355, .T. ) ;
#1243=CLOSED_SHELL ( 'NONE', ( #5729, #3388, #3751, #716, #4098, #5564 ) ) ;
#1280=CARTESIAN_POINT ( 'NONE',  ( -34.92499999999998295, 0.000000000000000000, 0.000000000000000000 ) ) ;
#1429=EDGE_LOOP ( 'NONE', ( #4529, #7281, #7580, #1167 ) ) ;
#1434=EDGE_CURVE ( 'NONE', #3827, #3933, #5578, .T. ) ;
#1468=APPLICATION_CONTEXT ( 'automotive_design' ) ;
#1506=DIRECTION ( 'NONE',  ( 0.000000000000000000, 0.000000000000000000, 1.000000000000000000 ) ) ;
#1613=DIRECTION ( 'NONE',  ( -1.000000000000000000, 0.000000000000000000, 0.000000000000000000 ) ) ;
#1636=ORIENTED_EDGE ( 'NONE', *, *, #7048, .T. ) ;
#1656=AXIS2_PLACEMENT_3D ( 'NONE', #7038, #8426, #1797 ) ;
#1677=EDGE_LOOP ( 'NONE', ( #1004, #1636 ) ) ;
#1797=DIRECTION ( 'NONE',  ( 0.000000000000000000, 0.000000000000000000, 1.000000000000000000 ) ) ;
#1801=VECTOR ( 'NONE', #1613, 1000.000000000000000 ) ;
#1802=MECHANICAL_DESIGN_GEOMETRIC_PRESENTATION_REPRESENTATION('',(#845),#2788);
#1880=CARTESIAN_POINT ( 'NONE',  ( 0.000000000000000000, 0.000000000000000000, 10.00000000000000178 ) ) ;
#1888=DIRECTION ( 'NONE',  ( 0.000000000000000000, 0.000000000000000000, 1.000000000000000000 ) ) ;
#1909=APPLICATION_CONTEXT ( 'automotive_design' ) ;
#1974=CIRCLE ( 'NONE', #580, 10.00000000000000178 ) ;
#2023=LINE ( 'NONE', #3324, #3942 ) ;
#2174=ORIENTED_EDGE ( 'NONE', *, *, #8270, .F. ) ;
#2215=CARTESIAN_POINT ( 'NONE',  ( 0.000000000000000000, 0.000000000000000000, 0.000000000000000000 ) ) ;
#2396=AXIS2_PLACEMENT_3D ( 'NONE', #1280, #7852, #1888 ) ;
#2418=CARTESIAN_POINT ( 'NONE',  ( -2.300000000000024247, 0.000000000000000000, 5.559999999999998721 ) ) ;
#2419=EDGE_CURVE ( 'NONE', #1055, #662, #691, .T. ) ;
#2423=DIRECTION ( 'NONE',  ( 0.000000000000000000, 0.000000000000000000, 1.000000000000000000 ) ) ;
#2521=ORIENTED_EDGE ( 'NONE', *, *, #592, .F. ) ;
#2557=ORIENTED_EDGE ( 'NONE', *, *, #7048, .F. ) ;
#2569=AXIS2_PLACEMENT_3D ( 'NONE', #7310, #5401, #8011 ) ;
#2746=( NAMED_UNIT ( * ) SI_UNIT ( $, .STERADIAN. ) SOLID_ANGLE_UNIT ( ) );
#2776=MANIFOLD_SOLID_BREP ( 'Base-Revolve', #1243 ) ;
#2777=DIRECTION ( 'NONE',  ( -1.000000000000000000, 0.000000000000000000, 0.000000000000000000 ) ) ;
#2788=( GEOMETRIC_REPRESENTATION_CONTEXT ( 3 ) GLOBAL_UNCERTAINTY_ASSIGNED_CONTEXT ( ( #7959 ) ) GLOBAL_UNIT_ASSIGNED_CONTEXT ( ( #7490, #6708, #2746 ) ) REPRESENTATION_CONTEXT ( 'NONE', 'WORKASPACE' ) );
#2792=EDGE_LOOP ( 'NONE', ( #2557, #7809, #2898, #4770 ) ) ;
#2815=FACE_OUTER_BOUND ( 'NONE', #5584, .T. ) ;
#2825=CARTESIAN_POINT ( 'NONE',  ( 0.000000000000000000, 0.000000000000000000, 0.000000000000000000 ) ) ;
#2858=EDGE_CURVE ( 'NONE', #5104, #3693, #1118, .T. ) ;
#2896=CYLINDRICAL_SURFACE ( 'NONE', #3922, 5.559999999999998721 ) ;
#2898=ORIENTED_EDGE ( 'NONE', *, *, #592, .T. ) ;
#3009=AXIS2_PLACEMENT_3D ( 'NONE', #814, #6696, #859 ) ;
#3067=( NAMED_UNIT ( * ) SI_UNIT ( $, .STERADIAN. ) SOLID_ANGLE_UNIT ( ) );
#3273=AXIS2_PLACEMENT_3D ( 'NONE', #8484, #1125, #6444 ) ;
#3324=CARTESIAN_POINT ( 'NONE',  ( -34.92499999999998295, 6.809036203259282560E-16, -5.559999999999998721 ) ) ;
#3337=ORIENTED_EDGE ( 'NONE', *, *, #7927, .F. ) ;
#3340=CARTESIAN_POINT ( 'NONE',  ( 0.000000000000000000, 1.224646799147353454E-15, -10.00000000000000178 ) ) ;
#3388=ADVANCED_FACE ( 'NONE', ( #7246 ), #6548, .F. ) ;
#3456=CYLINDRICAL_SURFACE ( 'NONE', #7055, 10.00000000000000178 ) ;
#3512=DIRECTION ( 'NONE',  ( 1.000000000000000000, 0.000000000000000000, 0.000000000000000000 ) ) ;
#3651=CARTESIAN_POINT ( 'NONE',  ( 0.000000000000000000, 0.000000000000000000, 5.559999999999998721 ) ) ;
#3688=( LENGTH_UNIT ( ) NAMED_UNIT ( * ) SI_UNIT ( .MILLI., .METRE. ) );
#3693=VERTEX_POINT ( 'NONE', #1880 ) ;
#3751=ADVANCED_FACE ( 'NONE', ( #2815 ), #2896, .F. ) ;
#3827=VERTEX_POINT ( 'NONE', #3651 ) ;
#3848=PRODUCT_DEFINITION_CONTEXT ( 'detailed design', #1909, 'design' ) ;
#3851=DIRECTION ( 'NONE',  ( -1.000000000000000000, 0.000000000000000000, 0.000000000000000000 ) ) ;
#3922=AXIS2_PLACEMENT_3D ( 'NONE', #194, #4824, #1506 ) ;
#3933=VERTEX_POINT ( 'NONE', #2418 ) ;
#3942=VECTOR ( 'NONE', #621, 1000.000000000000000 ) ;
#3956=EDGE_CURVE ( 'NONE', #1071, #6230, #2023, .T. ) ;
#4003=SHAPE_REPRESENTATION ( 'flat washer narrow_am_B18.22M - Plain washer, 10 mm, narrow', ( #7563 ), #4924 ) ;
#4012=SHAPE_DEFINITION_REPRESENTATION ( #4519, #4003 ) ;
#4027=AXIS2_PLACEMENT_3D ( 'NONE', #44, #89, #7244 ) ;
#4098=ADVANCED_FACE ( 'NONE', ( #6909 ), #762, .T. ) ;
#4151=CIRCLE ( 'NONE', #4847, 5.559999999999998721 ) ;
#4203=CARTESIAN_POINT ( 'NONE',  ( 0.000000000000000000, 0.000000000000000000, 0.000000000000000000 ) ) ;
#4228=CARTESIAN_POINT ( 'NONE',  ( -2.300000000000024247, 1.224646799147353454E-15, -10.00000000000000178 ) ) ;
#4235=EDGE_CURVE ( 'NONE', #5104, #1055, #5061, .T. ) ;
#4256=VECTOR ( 'NONE', #6320, 1000.000000000000000 ) ;
#4308=DIRECTION ( 'NONE',  ( 0.000000000000000000, 0.000000000000000000, 1.000000000000000000 ) ) ;
#4357=CIRCLE ( 'NONE', #7142, 5.559999999999998721 ) ;
#4506=CARTESIAN_POINT ( 'NONE',  ( 0.000000000000000000, 5.559999999999995168, 0.000000000000000000 ) ) ;
#4509=CARTESIAN_POINT ( 'NONE',  ( -2.300000000000024247, 0.000000000000000000, 0.000000000000000000 ) ) ;
#4519=PRODUCT_DEFINITION_SHAPE ( 'NONE', 'NONE',  #944 ) ;
#4529=ORIENTED_EDGE ( 'NONE', *, *, #4235, .F. ) ;
#4590=ORIENTED_EDGE ( 'NONE', *, *, #296, .F. ) ;
#4594=ORIENTED_EDGE ( 'NONE', *, *, #1173, .F. ) ;
#4600=DIRECTION ( 'NONE',  ( 0.000000000000000000, 0.000000000000000000, 1.000000000000000000 ) ) ;
#4639=AXIS2_PLACEMENT_3D ( 'NONE', #4506, #586, #4600 ) ;
#4678=DIRECTION ( 'NONE',  ( -1.000000000000000000, 0.000000000000000000, 0.000000000000000000 ) ) ;
#4770=ORIENTED_EDGE ( 'NONE', *, *, #1434, .F. ) ;
#4773=DIRECTION ( 'NONE',  ( -1.000000000000000000, 0.000000000000000000, 0.000000000000000000 ) ) ;
#4824=DIRECTION ( 'NONE',  ( -1.000000000000000000, 0.000000000000000000, 0.000000000000000000 ) ) ;
#4847=AXIS2_PLACEMENT_3D ( 'NONE', #2825, #8178, #7656 ) ;
#4900=PLANE ( 'NONE',  #3009 ) ;
#4924=( GEOMETRIC_REPRESENTATION_CONTEXT ( 3 ) GLOBAL_UNCERTAINTY_ASSIGNED_CONTEXT ( ( #5050 ) ) GLOBAL_UNIT_ASSIGNED_CONTEXT ( ( #3688, #376, #3067 ) ) REPRESENTATION_CONTEXT ( 'NONE', 'WORKASPACE' ) );
#5028=CARTESIAN_POINT ( 'NONE',  ( -2.300000000000024247, 0.000000000000000000, 10.00000000000000178 ) ) ;
#5050=UNCERTAINTY_MEASURE_WITH_UNIT (LENGTH_MEASURE( 1.000000000000000082E-05 ), #3688, 'distance_accuracy_value', 'NONE');
#5061=LINE ( 'NONE', #7638, #6726 ) ;
#5086=ORIENTED_EDGE ( 'NONE', *, *, #7702, .F. ) ;
#5097=PRODUCT_CONTEXT ( 'NONE', #1468, 'mechanical' ) ;
#5104=VERTEX_POINT ( 'NONE', #3340 ) ;
#5109=FACE_OUTER_BOUND ( 'NONE', #6465, .T. ) ;
#5328=CARTESIAN_POINT ( 'NONE',  ( -34.92499999999998295, 0.000000000000000000, 0.000000000000000000 ) ) ;
#5401=DIRECTION ( 'NONE',  ( -1.000000000000000000, 0.000000000000000000, 0.000000000000000000 ) ) ;
#5513=LINE ( 'NONE', #8075, #1801 ) ;
#5518=EDGE_LOOP ( 'NONE', ( #6983, #5601, #4590, #3337 ) ) ;
#5526=FACE_OUTER_BOUND ( 'NONE', #8299, .T. ) ;
#5564=ADVANCED_FACE ( 'NONE', ( #238, #5526 ), #4900, .F. ) ;
#5578=LINE ( 'NONE', #5628, #4256 ) ;
#5584=EDGE_LOOP ( 'NONE', ( #8400, #4594, #5925, #216 ) ) ;
#5601=ORIENTED_EDGE ( 'NONE', *, *, #4235, .T. ) ;
#5628=CARTESIAN_POINT ( 'NONE',  ( -34.92499999999998295, 0.000000000000000000, 5.559999999999998721 ) ) ;
#5650=CARTESIAN_POINT ( 'NONE',  ( -2.300000000000024247, 6.809036203259282560E-16, -5.559999999999998721 ) ) ;
#5704=DIRECTION ( 'NONE',  ( -1.000000000000000000, 0.000000000000000000, 0.000000000000000000 ) ) ;
#5729=ADVANCED_FACE ( 'NONE', ( #81 ), #3456, .T. ) ;
#5800=PRODUCT ( 'flat washer narrow_am_B18.22M - Plain washer, 10 mm, narrow', 'flat washer narrow_am_B18.22M - Plain washer, 10 mm, narrow', '', ( #5097 ) ) ;
#5925=ORIENTED_EDGE ( 'NONE', *, *, #1434, .T. ) ;
#5930=PRODUCT_DEFINITION_FORMATION_WITH_SPECIFIED_SOURCE ( 'ANY', '', #5800, .NOT_KNOWN. ) ;
#6136=CARTESIAN_POINT ( 'NONE',  ( -34.92499999999998295, 0.000000000000000000, 0.000000000000000000 ) ) ;
#6224=ORIENTED_EDGE ( 'NONE', *, *, #296, .T. ) ;
#6230=VERTEX_POINT ( 'NONE', #5650 ) ;
#6318=FACE_BOUND ( 'NONE', #1677, .T. ) ;
#6320=DIRECTION ( 'NONE',  ( -1.000000000000000000, 0.000000000000000000, 0.000000000000000000 ) ) ;
#6336=CIRCLE ( 'NONE', #2569, 10.00000000000000178 ) ;
#6444=DIRECTION ( 'NONE',  ( 0.000000000000000000, 0.000000000000000000, 1.000000000000000000 ) ) ;
#6464=SHAPE_REPRESENTATION_RELATIONSHIP ( 'NONE' , 'NONE' ,  #4003, #841 ) ;
#6465=EDGE_LOOP ( 'NONE', ( #2174, #275 ) ) ;
#6548=CYLINDRICAL_SURFACE ( 'NONE', #2396, 5.559999999999998721 ) ;
#6696=DIRECTION ( 'NONE',  ( 1.000000000000000000, 0.000000000000000000, 0.000000000000000000 ) ) ;
#6708=( NAMED_UNIT ( * ) PLANE_ANGLE_UNIT ( ) SI_UNIT ( $, .RADIAN. ) );
#6726=VECTOR ( 'NONE', #5704, 1000.000000000000000 ) ;
#6909=FACE_OUTER_BOUND ( 'NONE', #1429, .T. ) ;
#6977=DIRECTION ( 'NONE',  ( -1.000000000000000000, 0.000000000000000000, 0.000000000000000000 ) ) ;
#6983=ORIENTED_EDGE ( 'NONE', *, *, #8270, .T. ) ;
#6984=EDGE_LOOP ( 'NONE', ( #5086, #2521 ) ) ;
#7038=CARTESIAN_POINT ( 'NONE',  ( -2.300000000000024247, 0.000000000000000000, 0.000000000000000000 ) ) ;
#7048=EDGE_CURVE ( 'NONE', #1071, #3827, #4151, .T. ) ;
#7055=AXIS2_PLACEMENT_3D ( 'NONE', #5328, #4678, #130 ) ;
#7142=AXIS2_PLACEMENT_3D ( 'NONE', #107, #2777, #155 ) ;
#7233=CIRCLE ( 'NONE', #1656, 5.559999999999998721 ) ;
#7244=DIRECTION ( 'NONE',  ( 0.000000000000000000, 0.000000000000000000, 1.000000000000000000 ) ) ;
#7246=FACE_OUTER_BOUND ( 'NONE', #2792, .T. ) ;
#7268=ORIENTED_EDGE ( 'NONE', *, *, #2419, .T. ) ;
#7281=ORIENTED_EDGE ( 'NONE', *, *, #2858, .T. ) ;
#7310=CARTESIAN_POINT ( 'NONE',  ( 0.000000000000000000, 0.000000000000000000, 0.000000000000000000 ) ) ;
#7478=DIRECTION ( 'NONE',  ( 0.000000000000000000, 0.000000000000000000, 1.000000000000000000 ) ) ;
#7490=( LENGTH_UNIT ( ) NAMED_UNIT ( * ) SI_UNIT ( .MILLI., .METRE. ) );
#7563=AXIS2_PLACEMENT_3D ( 'NONE', #4203, #7478, #3512 ) ;
#7580=ORIENTED_EDGE ( 'NONE', *, *, #7927, .T. ) ;
#7638=CARTESIAN_POINT ( 'NONE',  ( -34.92499999999998295, 1.224646799147353454E-15, -10.00000000000000178 ) ) ;
#7656=DIRECTION ( 'NONE',  ( 0.000000000000000000, 0.000000000000000000, 1.000000000000000000 ) ) ;
#7702=EDGE_CURVE ( 'NONE', #3933, #6230, #7233, .T. ) ;
#7768=PLANE ( 'NONE',  #4639 ) ;
#7809=ORIENTED_EDGE ( 'NONE', *, *, #3956, .T. ) ;
#7852=DIRECTION ( 'NONE',  ( -1.000000000000000000, 0.000000000000000000, 0.000000000000000000 ) ) ;
#7927=EDGE_CURVE ( 'NONE', #3693, #662, #5513, .T. ) ;
#7959=UNCERTAINTY_MEASURE_WITH_UNIT (LENGTH_MEASURE( 1.000000000000000082E-05 ), #7490, 'distance_accuracy_value', 'NONE');
#8011=DIRECTION ( 'NONE',  ( 0.000000000000000000, 0.000000000000000000, 1.000000000000000000 ) ) ;
#8075=CARTESIAN_POINT ( 'NONE',  ( -34.92499999999998295, 0.000000000000000000, 10.00000000000000178 ) ) ;
#8079=AXIS2_PLACEMENT_3D ( 'NONE', #2215, #6977, #4308 ) ;
#8178=DIRECTION ( 'NONE',  ( -1.000000000000000000, 0.000000000000000000, 0.000000000000000000 ) ) ;
#8236=CARTESIAN_POINT ( 'NONE',  ( 0.000000000000000000, 6.809036203259282560E-16, -5.559999999999998721 ) ) ;
#8270=EDGE_CURVE ( 'NONE', #3693, #5104, #6336, .T. ) ;
#8299=EDGE_LOOP ( 'NONE', ( #6224, #7268 ) ) ;
#8377=AXIS2_PLACEMENT_3D ( 'NONE', #6136, #4773, #143 ) ;
#8400=ORIENTED_EDGE ( 'NONE', *, *, #3956, .F. ) ;
#8426=DIRECTION ( 'NONE',  ( -1.000000000000000000, 0.000000000000000000, 0.000000000000000000 ) ) ;
#8484=CARTESIAN_POINT ( 'NONE',  ( 0.000000000000000000, 0.000000000000000000, 0.000000000000000000 ) ) ;
#8664=COLOUR_RGB('Black',0.12,0.14,0.17);
#8665=FILL_AREA_STYLE_COLOUR('',#8664);
#8666=FILL_AREA_STYLE('',(#8665));
#8667=SURFACE_STYLE_FILL_AREA(#8666);
#8668=SURFACE_SIDE_STYLE('',(#8667));
#8669=SURFACE_STYLE_USAGE(.BOTH.,#8668);
#8670=PRESENTATION_STYLE_ASSIGNMENT((#8669));
ENDSEC;
END-ISO-10303-21;
